ISO-10303-21;
HEADER;
/* Generated by software containing ST-Developer
 * from STEP Tools, Inc. (www.steptools.com) 
 */

FILE_DESCRIPTION(
/* description */ ('Manifold and mounting hardware'),
/* implementation_level */ '2;1');

FILE_NAME(
/* name */ '1_4-1_8 in port reducer.step',
/* time_stamp */ '2026-10-28T21:46:49-07:00',
/* author */ (''),
/* organization */ (''),
/* preprocessor_version */ 'ST-DEVELOPER v20.2',
/* originating_system */ 'Autodesk Translation Framework v15.17.0.0',
/* authorisation */ '');

FILE_SCHEMA (('AUTOMOTIVE_DESIGN { 1 0 10303 214 3 1 1 }'));
ENDSEC;

DATA;
#10=MECHANICAL_DESIGN_GEOMETRIC_PRESENTATION_REPRESENTATION('',(#152),#5638);
#124=SHAPE_REPRESENTATION_RELATIONSHIP('SRR','None',#5703,#138);
#138=ADVANCED_BREP_SHAPE_REPRESENTATION('',(#166),#5625);
#152=STYLED_ITEM('',(#5853),#166);
#166=MANIFOLD_SOLID_BREP('Body1',#3142);
#200=FACE_BOUND('',#590,.T.);
#201=FACE_BOUND('',#592,.T.);
#202=FACE_BOUND('',#600,.T.);
#203=FACE_BOUND('',#604,.T.);
#291=CYLINDRICAL_SURFACE('',#3417,0.515);
#292=CYLINDRICAL_SURFACE('',#3431,0.2);
#293=CYLINDRICAL_SURFACE('',#3433,0.685);
#380=FACE_OUTER_BOUND('',#588,.T.);
#381=FACE_OUTER_BOUND('',#589,.T.);
#382=FACE_OUTER_BOUND('',#591,.T.);
#383=FACE_OUTER_BOUND('',#593,.T.);
#384=FACE_OUTER_BOUND('',#594,.T.);
#385=FACE_OUTER_BOUND('',#595,.T.);
#386=FACE_OUTER_BOUND('',#596,.T.);
#387=FACE_OUTER_BOUND('',#597,.T.);
#388=FACE_OUTER_BOUND('',#598,.T.);
#389=FACE_OUTER_BOUND('',#599,.T.);
#390=FACE_OUTER_BOUND('',#601,.T.);
#391=FACE_OUTER_BOUND('',#602,.T.);
#392=FACE_OUTER_BOUND('',#603,.T.);
#588=EDGE_LOOP('',(#2280,#2281,#2282,#2283));
#589=EDGE_LOOP('',(#2284));
#590=EDGE_LOOP('',(#2285));
#591=EDGE_LOOP('',(#2286,#2287,#2288,#2289,#2290,#2291));
#592=EDGE_LOOP('',(#2292));
#593=EDGE_LOOP('',(#2293,#2294,#2295,#2296));
#594=EDGE_LOOP('',(#2297,#2298,#2299,#2300));
#595=EDGE_LOOP('',(#2301,#2302,#2303,#2304));
#596=EDGE_LOOP('',(#2305,#2306,#2307,#2308));
#597=EDGE_LOOP('',(#2309,#2310,#2311,#2312));
#598=EDGE_LOOP('',(#2313,#2314,#2315,#2316));
#599=EDGE_LOOP('',(#2317,#2318,#2319,#2320,#2321,#2322));
#600=EDGE_LOOP('',(#2323));
#601=EDGE_LOOP('',(#2324,#2325,#2326,#2327));
#602=EDGE_LOOP('',(#2328,#2329,#2330,#2331));
#603=EDGE_LOOP('',(#2332));
#604=EDGE_LOOP('',(#2333));
#815=CIRCLE('',#3418,0.515);
#816=CIRCLE('',#3419,0.515);
#817=CIRCLE('',#3421,0.2);
#818=CIRCLE('',#3423,0.685);
#819=CIRCLE('',#3432,0.2);
#820=CIRCLE('',#3434,0.685);
#957=LINE('',#4967,#1204);
#958=LINE('',#4975,#1205);
#959=LINE('',#4977,#1206);
#960=LINE('',#4979,#1207);
#961=LINE('',#4981,#1208);
#962=LINE('',#4983,#1209);
#963=LINE('',#4984,#1210);
#964=LINE('',#4989,#1211);
#965=LINE('',#4991,#1212);
#966=LINE('',#4992,#1213);
#967=LINE('',#4995,#1214);
#968=LINE('',#4996,#1215);
#969=LINE('',#4999,#1216);
#970=LINE('',#5000,#1217);
#971=LINE('',#5003,#1218);
#972=LINE('',#5004,#1219);
#973=LINE('',#5007,#1220);
#974=LINE('',#5008,#1221);
#975=LINE('',#5010,#1222);
#976=LINE('',#5014,#1223);
#977=LINE('',#5018,#1224);
#1204=VECTOR('',#3952,0.515);
#1205=VECTOR('',#3961,1.);
#1206=VECTOR('',#3962,1.);
#1207=VECTOR('',#3963,1.);
#1208=VECTOR('',#3964,1.);
#1209=VECTOR('',#3965,1.);
#1210=VECTOR('',#3966,1.);
#1211=VECTOR('',#3971,1.);
#1212=VECTOR('',#3972,1.);
#1213=VECTOR('',#3973,1.);
#1214=VECTOR('',#3976,1.);
#1215=VECTOR('',#3977,1.);
#1216=VECTOR('',#3980,1.);
#1217=VECTOR('',#3981,1.);
#1218=VECTOR('',#3984,1.);
#1219=VECTOR('',#3985,1.);
#1220=VECTOR('',#3988,1.);
#1221=VECTOR('',#3989,1.);
#1222=VECTOR('',#3992,1.);
#1223=VECTOR('',#3997,0.2);
#1224=VECTOR('',#4002,0.685);
#1469=VERTEX_POINT('',#4964);
#1470=VERTEX_POINT('',#4966);
#1471=VERTEX_POINT('',#4970);
#1472=VERTEX_POINT('',#4973);
#1473=VERTEX_POINT('',#4974);
#1474=VERTEX_POINT('',#4976);
#1475=VERTEX_POINT('',#4978);
#1476=VERTEX_POINT('',#4980);
#1477=VERTEX_POINT('',#4982);
#1478=VERTEX_POINT('',#4985);
#1479=VERTEX_POINT('',#4988);
#1480=VERTEX_POINT('',#4990);
#1481=VERTEX_POINT('',#4994);
#1482=VERTEX_POINT('',#4998);
#1483=VERTEX_POINT('',#5002);
#1484=VERTEX_POINT('',#5006);
#1485=VERTEX_POINT('',#5013);
#1486=VERTEX_POINT('',#5017);
#1769=EDGE_CURVE('',#1469,#1469,#815,.T.);
#1770=EDGE_CURVE('',#1469,#1470,#957,.T.);
#1771=EDGE_CURVE('',#1470,#1470,#816,.T.);
#1772=EDGE_CURVE('',#1471,#1471,#817,.T.);
#1773=EDGE_CURVE('',#1472,#1473,#958,.T.);
#1774=EDGE_CURVE('',#1474,#1472,#959,.T.);
#1775=EDGE_CURVE('',#1475,#1474,#960,.T.);
#1776=EDGE_CURVE('',#1476,#1475,#961,.T.);
#1777=EDGE_CURVE('',#1477,#1476,#962,.T.);
#1778=EDGE_CURVE('',#1473,#1477,#963,.T.);
#1779=EDGE_CURVE('',#1478,#1478,#818,.T.);
#1780=EDGE_CURVE('',#1472,#1479,#964,.T.);
#1781=EDGE_CURVE('',#1480,#1479,#965,.T.);
#1782=EDGE_CURVE('',#1474,#1480,#966,.T.);
#1783=EDGE_CURVE('',#1481,#1480,#967,.T.);
#1784=EDGE_CURVE('',#1475,#1481,#968,.T.);
#1785=EDGE_CURVE('',#1482,#1481,#969,.T.);
#1786=EDGE_CURVE('',#1476,#1482,#970,.T.);
#1787=EDGE_CURVE('',#1483,#1482,#971,.T.);
#1788=EDGE_CURVE('',#1477,#1483,#972,.T.);
#1789=EDGE_CURVE('',#1484,#1483,#973,.T.);
#1790=EDGE_CURVE('',#1473,#1484,#974,.T.);
#1791=EDGE_CURVE('',#1479,#1484,#975,.T.);
#1792=EDGE_CURVE('',#1471,#1485,#976,.T.);
#1793=EDGE_CURVE('',#1485,#1485,#819,.T.);
#1794=EDGE_CURVE('',#1478,#1486,#977,.T.);
#1795=EDGE_CURVE('',#1486,#1486,#820,.T.);
#2280=ORIENTED_EDGE('',*,*,#1769,.F.);
#2281=ORIENTED_EDGE('',*,*,#1770,.T.);
#2282=ORIENTED_EDGE('',*,*,#1771,.F.);
#2283=ORIENTED_EDGE('',*,*,#1770,.F.);
#2284=ORIENTED_EDGE('',*,*,#1769,.T.);
#2285=ORIENTED_EDGE('',*,*,#1772,.F.);
#2286=ORIENTED_EDGE('',*,*,#1773,.F.);
#2287=ORIENTED_EDGE('',*,*,#1774,.F.);
#2288=ORIENTED_EDGE('',*,*,#1775,.F.);
#2289=ORIENTED_EDGE('',*,*,#1776,.F.);
#2290=ORIENTED_EDGE('',*,*,#1777,.F.);
#2291=ORIENTED_EDGE('',*,*,#1778,.F.);
#2292=ORIENTED_EDGE('',*,*,#1779,.T.);
#2293=ORIENTED_EDGE('',*,*,#1774,.T.);
#2294=ORIENTED_EDGE('',*,*,#1780,.T.);
#2295=ORIENTED_EDGE('',*,*,#1781,.F.);
#2296=ORIENTED_EDGE('',*,*,#1782,.F.);
#2297=ORIENTED_EDGE('',*,*,#1775,.T.);
#2298=ORIENTED_EDGE('',*,*,#1782,.T.);
#2299=ORIENTED_EDGE('',*,*,#1783,.F.);
#2300=ORIENTED_EDGE('',*,*,#1784,.F.);
#2301=ORIENTED_EDGE('',*,*,#1776,.T.);
#2302=ORIENTED_EDGE('',*,*,#1784,.T.);
#2303=ORIENTED_EDGE('',*,*,#1785,.F.);
#2304=ORIENTED_EDGE('',*,*,#1786,.F.);
#2305=ORIENTED_EDGE('',*,*,#1777,.T.);
#2306=ORIENTED_EDGE('',*,*,#1786,.T.);
#2307=ORIENTED_EDGE('',*,*,#1787,.F.);
#2308=ORIENTED_EDGE('',*,*,#1788,.F.);
#2309=ORIENTED_EDGE('',*,*,#1778,.T.);
#2310=ORIENTED_EDGE('',*,*,#1788,.T.);
#2311=ORIENTED_EDGE('',*,*,#1789,.F.);
#2312=ORIENTED_EDGE('',*,*,#1790,.F.);
#2313=ORIENTED_EDGE('',*,*,#1773,.T.);
#2314=ORIENTED_EDGE('',*,*,#1790,.T.);
#2315=ORIENTED_EDGE('',*,*,#1791,.F.);
#2316=ORIENTED_EDGE('',*,*,#1780,.F.);
#2317=ORIENTED_EDGE('',*,*,#1791,.T.);
#2318=ORIENTED_EDGE('',*,*,#1789,.T.);
#2319=ORIENTED_EDGE('',*,*,#1787,.T.);
#2320=ORIENTED_EDGE('',*,*,#1785,.T.);
#2321=ORIENTED_EDGE('',*,*,#1783,.T.);
#2322=ORIENTED_EDGE('',*,*,#1781,.T.);
#2323=ORIENTED_EDGE('',*,*,#1771,.T.);
#2324=ORIENTED_EDGE('',*,*,#1772,.T.);
#2325=ORIENTED_EDGE('',*,*,#1792,.T.);
#2326=ORIENTED_EDGE('',*,*,#1793,.T.);
#2327=ORIENTED_EDGE('',*,*,#1792,.F.);
#2328=ORIENTED_EDGE('',*,*,#1779,.F.);
#2329=ORIENTED_EDGE('',*,*,#1794,.T.);
#2330=ORIENTED_EDGE('',*,*,#1795,.T.);
#2331=ORIENTED_EDGE('',*,*,#1794,.F.);
#2332=ORIENTED_EDGE('',*,*,#1795,.F.);
#2333=ORIENTED_EDGE('',*,*,#1793,.F.);
#2862=PLANE('',#3420);
#2863=PLANE('',#3422);
#2864=PLANE('',#3424);
#2865=PLANE('',#3425);
#2866=PLANE('',#3426);
#2867=PLANE('',#3427);
#2868=PLANE('',#3428);
#2869=PLANE('',#3429);
#2870=PLANE('',#3430);
#2871=PLANE('',#3435);
#3004=ADVANCED_FACE('',(#380),#291,.F.);
#3005=ADVANCED_FACE('',(#381,#200),#2862,.T.);
#3006=ADVANCED_FACE('',(#382,#201),#2863,.F.);
#3007=ADVANCED_FACE('',(#383),#2864,.T.);
#3008=ADVANCED_FACE('',(#384),#2865,.T.);
#3009=ADVANCED_FACE('',(#385),#2866,.T.);
#3010=ADVANCED_FACE('',(#386),#2867,.T.);
#3011=ADVANCED_FACE('',(#387),#2868,.T.);
#3012=ADVANCED_FACE('',(#388),#2869,.T.);
#3013=ADVANCED_FACE('',(#389,#202),#2870,.T.);
#3014=ADVANCED_FACE('',(#390),#292,.F.);
#3015=ADVANCED_FACE('',(#391),#293,.T.);
#3016=ADVANCED_FACE('',(#392,#203),#2871,.F.);
#3142=CLOSED_SHELL('',(#3004,#3005,#3006,#3007,#3008,#3009,#3010,#3011,
#3012,#3013,#3014,#3015,#3016));
#3416=AXIS2_PLACEMENT_3D('',#4962,#3946,#3947);
#3417=AXIS2_PLACEMENT_3D('',#4963,#3948,#3949);
#3418=AXIS2_PLACEMENT_3D('',#4965,#3950,#3951);
#3419=AXIS2_PLACEMENT_3D('',#4968,#3953,#3954);
#3420=AXIS2_PLACEMENT_3D('',#4969,#3955,#3956);
#3421=AXIS2_PLACEMENT_3D('',#4971,#3957,#3958);
#3422=AXIS2_PLACEMENT_3D('',#4972,#3959,#3960);
#3423=AXIS2_PLACEMENT_3D('',#4986,#3967,#3968);
#3424=AXIS2_PLACEMENT_3D('',#4987,#3969,#3970);
#3425=AXIS2_PLACEMENT_3D('',#4993,#3974,#3975);
#3426=AXIS2_PLACEMENT_3D('',#4997,#3978,#3979);
#3427=AXIS2_PLACEMENT_3D('',#5001,#3982,#3983);
#3428=AXIS2_PLACEMENT_3D('',#5005,#3986,#3987);
#3429=AXIS2_PLACEMENT_3D('',#5009,#3990,#3991);
#3430=AXIS2_PLACEMENT_3D('',#5011,#3993,#3994);
#3431=AXIS2_PLACEMENT_3D('',#5012,#3995,#3996);
#3432=AXIS2_PLACEMENT_3D('',#5015,#3998,#3999);
#3433=AXIS2_PLACEMENT_3D('',#5016,#4000,#4001);
#3434=AXIS2_PLACEMENT_3D('',#5019,#4003,#4004);
#3435=AXIS2_PLACEMENT_3D('',#5020,#4005,#4006);
#3946=DIRECTION('axis',(0.,0.,1.));
#3947=DIRECTION('refdir',(1.,0.,0.));
#3948=DIRECTION('center_axis',(0.,0.,1.));
#3949=DIRECTION('ref_axis',(1.,0.,0.));
#3950=DIRECTION('center_axis',(0.,0.,1.));
#3951=DIRECTION('ref_axis',(1.,0.,0.));
#3952=DIRECTION('',(0.,0.,1.));
#3953=DIRECTION('center_axis',(0.,0.,-1.));
#3954=DIRECTION('ref_axis',(1.,0.,0.));
#3955=DIRECTION('center_axis',(0.,0.,1.));
#3956=DIRECTION('ref_axis',(1.,0.,0.));
#3957=DIRECTION('center_axis',(0.,0.,1.));
#3958=DIRECTION('ref_axis',(1.,0.,0.));
#3959=DIRECTION('center_axis',(0.,0.,1.));
#3960=DIRECTION('ref_axis',(1.,0.,0.));
#3961=DIRECTION('',(0.5,0.866025403784439,0.));
#3962=DIRECTION('',(1.,-3.29650746237182E-16,0.));
#3963=DIRECTION('',(0.5,-0.866025403784439,0.));
#3964=DIRECTION('',(-0.500000000000001,-0.866025403784438,0.));
#3965=DIRECTION('',(-1.,0.,0.));
#3966=DIRECTION('',(-0.5,0.866025403784439,0.));
#3967=DIRECTION('center_axis',(0.,0.,1.));
#3968=DIRECTION('ref_axis',(1.,0.,0.));
#3969=DIRECTION('center_axis',(-3.29650746237182E-16,-1.,0.));
#3970=DIRECTION('ref_axis',(1.,-3.29650746237182E-16,0.));
#3971=DIRECTION('',(0.,0.,1.));
#3972=DIRECTION('',(1.,-3.29650746237182E-16,0.));
#3973=DIRECTION('',(0.,0.,1.));
#3974=DIRECTION('center_axis',(-0.866025403784439,-0.5,0.));
#3975=DIRECTION('ref_axis',(0.5,-0.866025403784439,0.));
#3976=DIRECTION('',(0.5,-0.866025403784439,0.));
#3977=DIRECTION('',(0.,0.,1.));
#3978=DIRECTION('center_axis',(-0.866025403784438,0.500000000000001,0.));
#3979=DIRECTION('ref_axis',(-0.500000000000001,-0.866025403784438,0.));
#3980=DIRECTION('',(-0.500000000000001,-0.866025403784438,0.));
#3981=DIRECTION('',(0.,0.,1.));
#3982=DIRECTION('center_axis',(0.,1.,0.));
#3983=DIRECTION('ref_axis',(-1.,0.,0.));
#3984=DIRECTION('',(-1.,0.,0.));
#3985=DIRECTION('',(0.,0.,1.));
#3986=DIRECTION('center_axis',(0.866025403784439,0.5,0.));
#3987=DIRECTION('ref_axis',(-0.5,0.866025403784439,0.));
#3988=DIRECTION('',(-0.5,0.866025403784439,0.));
#3989=DIRECTION('',(0.,0.,1.));
#3990=DIRECTION('center_axis',(0.866025403784439,-0.5,0.));
#3991=DIRECTION('ref_axis',(0.5,0.866025403784439,0.));
#3992=DIRECTION('',(0.5,0.866025403784439,0.));
#3993=DIRECTION('center_axis',(0.,0.,1.));
#3994=DIRECTION('ref_axis',(1.,0.,0.));
#3995=DIRECTION('center_axis',(0.,0.,1.));
#3996=DIRECTION('ref_axis',(1.,0.,0.));
#3997=DIRECTION('',(0.,0.,-1.));
#3998=DIRECTION('center_axis',(0.,0.,-1.));
#3999=DIRECTION('ref_axis',(1.,0.,0.));
#4000=DIRECTION('center_axis',(0.,0.,1.));
#4001=DIRECTION('ref_axis',(1.,0.,0.));
#4002=DIRECTION('',(0.,0.,-1.));
#4003=DIRECTION('center_axis',(0.,0.,1.));
#4004=DIRECTION('ref_axis',(1.,0.,0.));
#4005=DIRECTION('center_axis',(0.,0.,1.));
#4006=DIRECTION('ref_axis',(1.,0.,0.));
#4962=CARTESIAN_POINT('',(0.,0.,0.));
#4963=CARTESIAN_POINT('Origin',(-1.25,0.,4.85));
#4964=CARTESIAN_POINT('',(-1.765,-6.30693101560887E-17,4.85));
#4965=CARTESIAN_POINT('Origin',(-1.25,0.,4.85));
#4966=CARTESIAN_POINT('',(-1.765,6.30693101560887E-17,5.5));
#4967=CARTESIAN_POINT('',(-1.765,-6.30693101560887E-17,4.85));
#4968=CARTESIAN_POINT('Origin',(-1.25,0.,5.5));
#4969=CARTESIAN_POINT('Origin',(-1.25,0.,4.85));
#4970=CARTESIAN_POINT('',(-1.45,-2.44929359829471E-17,4.85));
#4971=CARTESIAN_POINT('Origin',(-1.25,0.,4.85));
#4972=CARTESIAN_POINT('Origin',(-1.25,0.,5.));
#4973=CARTESIAN_POINT('',(-0.744818514459077,-0.875,5.));
#4974=CARTESIAN_POINT('',(-0.239637028918155,0.,5.));
#4975=CARTESIAN_POINT('',(-0.744818514459077,-0.875,5.));
#4976=CARTESIAN_POINT('',(-1.75518148554092,-0.875,5.));
#4977=CARTESIAN_POINT('',(-1.75518148554092,-0.875,5.));
#4978=CARTESIAN_POINT('',(-2.26036297108185,1.23733777851239E-16,5.));
#4979=CARTESIAN_POINT('',(-2.26036297108185,1.23733777851239E-16,5.));
#4980=CARTESIAN_POINT('',(-1.75518148554092,0.875,5.));
#4981=CARTESIAN_POINT('',(-1.75518148554092,0.875,5.));
#4982=CARTESIAN_POINT('',(-0.744818514459077,0.875,5.));
#4983=CARTESIAN_POINT('',(-0.744818514459077,0.875,5.));
#4984=CARTESIAN_POINT('',(-0.239637028918155,0.,5.));
#4985=CARTESIAN_POINT('',(-1.935,-8.38883057415937E-17,5.));
#4986=CARTESIAN_POINT('Origin',(-1.25,0.,5.));
#4987=CARTESIAN_POINT('Origin',(-1.75518148554092,-0.875,5.));
#4988=CARTESIAN_POINT('',(-0.744818514459077,-0.875,5.5));
#4989=CARTESIAN_POINT('',(-0.744818514459077,-0.875,5.));
#4990=CARTESIAN_POINT('',(-1.75518148554092,-0.875,5.5));
#4991=CARTESIAN_POINT('',(-1.75518148554092,-0.875,5.5));
#4992=CARTESIAN_POINT('',(-1.75518148554092,-0.875,5.));
#4993=CARTESIAN_POINT('Origin',(-2.26036297108185,1.23733777851239E-16,
5.));
#4994=CARTESIAN_POINT('',(-2.26036297108185,1.11022302462516E-16,5.5));
#4995=CARTESIAN_POINT('',(-2.26036297108185,1.23733777851239E-16,5.5));
#4996=CARTESIAN_POINT('',(-2.26036297108185,1.23733777851239E-16,5.));
#4997=CARTESIAN_POINT('Origin',(-1.75518148554092,0.875,5.));
#4998=CARTESIAN_POINT('',(-1.75518148554092,0.875,5.5));
#4999=CARTESIAN_POINT('',(-1.75518148554092,0.875,5.5));
#5000=CARTESIAN_POINT('',(-1.75518148554092,0.875,5.));
#5001=CARTESIAN_POINT('Origin',(-0.744818514459077,0.875,5.));
#5002=CARTESIAN_POINT('',(-0.744818514459077,0.875,5.5));
#5003=CARTESIAN_POINT('',(-0.744818514459077,0.875,5.5));
#5004=CARTESIAN_POINT('',(-0.744818514459077,0.875,5.));
#5005=CARTESIAN_POINT('Origin',(-0.239637028918155,0.,5.));
#5006=CARTESIAN_POINT('',(-0.239637028918155,0.,5.5));
#5007=CARTESIAN_POINT('',(-0.239637028918155,0.,5.5));
#5008=CARTESIAN_POINT('',(-0.239637028918155,0.,5.));
#5009=CARTESIAN_POINT('Origin',(-0.744818514459077,-0.875,5.));
#5010=CARTESIAN_POINT('',(-0.744818514459077,-0.875,5.5));
#5011=CARTESIAN_POINT('Origin',(-1.25,0.,5.5));
#5012=CARTESIAN_POINT('Origin',(-1.25,0.,3.8));
#5013=CARTESIAN_POINT('',(-1.45,-2.44929359829471E-17,3.8));
#5014=CARTESIAN_POINT('',(-1.45,-2.44929359829471E-17,3.8));
#5015=CARTESIAN_POINT('Origin',(-1.25,0.,3.8));
#5016=CARTESIAN_POINT('Origin',(-1.25,0.,3.8));
#5017=CARTESIAN_POINT('',(-1.935,-8.38883057415937E-17,3.8));
#5018=CARTESIAN_POINT('',(-1.935,-8.38883057415937E-17,3.8));
#5019=CARTESIAN_POINT('Origin',(-1.25,0.,3.8));
#5020=CARTESIAN_POINT('Origin',(-1.25,0.,3.8));
#5608=UNCERTAINTY_MEASURE_WITH_UNIT(LENGTH_MEASURE(0.001),#5639,
'DISTANCE_ACCURACY_VALUE',
'Maximum model space distance between geometric entities at asserted c
onnectivities');
#5621=UNCERTAINTY_MEASURE_WITH_UNIT(LENGTH_MEASURE(0.001),#5639,
'DISTANCE_ACCURACY_VALUE',
'Maximum model space distance between geometric entities at asserted c
onnectivities');
#5625=(
GEOMETRIC_REPRESENTATION_CONTEXT(3)
GLOBAL_UNCERTAINTY_ASSIGNED_CONTEXT((#5608))
GLOBAL_UNIT_ASSIGNED_CONTEXT((#5639,#5641,#5642))
REPRESENTATION_CONTEXT('','3D')
);
#5638=(
GEOMETRIC_REPRESENTATION_CONTEXT(3)
GLOBAL_UNCERTAINTY_ASSIGNED_CONTEXT((#5621))
GLOBAL_UNIT_ASSIGNED_CONTEXT((#5639,#5641,#5642))
REPRESENTATION_CONTEXT('','3D')
);
#5639=(
LENGTH_UNIT()
NAMED_UNIT(*)
SI_UNIT(.CENTI.,.METRE.)
);
#5641=(
NAMED_UNIT(*)
PLANE_ANGLE_UNIT()
SI_UNIT($,.RADIAN.)
);
#5642=(
NAMED_UNIT(*)
SI_UNIT($,.STERADIAN.)
SOLID_ANGLE_UNIT()
);
#5646=SHAPE_DEFINITION_REPRESENTATION(#5662,#5703);
#5662=PRODUCT_DEFINITION_SHAPE('',$,#5720);
#5703=SHAPE_REPRESENTATION('',(#3416),#5625);
#5716=PRODUCT_DEFINITION_CONTEXT('part definition',#5766,'design');
#5720=PRODUCT_DEFINITION('1/4-1/8 in port reducer',
'1/4-1/8 in port reducer',#5736,#5716);
#5736=PRODUCT_DEFINITION_FORMATION('',$,#5771);
#5766=APPLICATION_CONTEXT(
'Core Data for Automotive Mechanical Design Process');
#5767=PRODUCT_CONTEXT('part definition',#5766,'mechanical');
#5771=PRODUCT('1/4-1/8 in port reducer','1/4-1/8 in port reducer',
'1/4-1/8 in port reducer',(#5767));
#5847=COLOUR_RGB('Sky Blue',0.24,0.69,0.87);
#5848=FILL_AREA_STYLE_COLOUR('',#5847);
#5849=FILL_AREA_STYLE('',(#5848));
#5850=SURFACE_STYLE_FILL_AREA(#5849);
#5851=SURFACE_SIDE_STYLE('',(#5850));
#5852=SURFACE_STYLE_USAGE(.BOTH.,#5851);
#5853=PRESENTATION_STYLE_ASSIGNMENT((#5852));
ENDSEC;
END-ISO-10303-21;
